ISO-10303-21;
HEADER;
/* Generated by software containing ST-Developer
 * from STEP Tools, Inc. (www.steptools.com) 
 */

FILE_DESCRIPTION(
/* description */ (''),
/* implementation_level */ '2;1');

FILE_NAME(
/* name */ 'Screw.step',
/* time_stamp */ '2026-10-19T01:30:23+06:00',
/* author */ (''),
/* organization */ (''),
/* preprocessor_version */ 'ST-DEVELOPER v20.2',
/* originating_system */ 'Autodesk Translation Framework v15.15.0.0',
/* authorisation */ '');

FILE_SCHEMA (('AUTOMOTIVE_DESIGN { 1 0 10303 214 3 1 1 }'));
ENDSEC;

DATA;
#10=MECHANICAL_DESIGN_GEOMETRIC_PRESENTATION_REPRESENTATION('',(#91),#10639);
#71=SHAPE_REPRESENTATION_RELATIONSHIP('SRR','None',#10681,#81);
#81=ADVANCED_BREP_SHAPE_REPRESENTATION('',(#101),#10633);
#91=STYLED_ITEM('',(#10797),#101);
#101=MANIFOLD_SOLID_BREP('Screw',#5717);
#357=PLANE('',#6422);
#358=PLANE('',#6426);
#651=FACE_OUTER_BOUND('',#1073,.T.);
#652=FACE_OUTER_BOUND('',#1074,.T.);
#653=FACE_OUTER_BOUND('',#1075,.T.);
#1073=EDGE_LOOP('',(#4666));
#1074=EDGE_LOOP('',(#4667,#4668,#4669,#4670));
#1075=EDGE_LOOP('',(#4671));
#1439=LINE('',#10005,#1769);
#1769=VECTOR('',#8115,5.);
#2162=CIRCLE('',#6423,4.925);
#2163=CIRCLE('',#6425,4.925);
#2616=VERTEX_POINT('',#10000);
#2617=VERTEX_POINT('',#10003);
#3309=EDGE_CURVE('',#2616,#2616,#2162,.T.);
#3310=EDGE_CURVE('',#2617,#2617,#2163,.F.);
#3311=EDGE_CURVE('',#2617,#2616,#1439,.T.);
#4666=ORIENTED_EDGE('',*,*,#3309,.T.);
#4667=ORIENTED_EDGE('',*,*,#3310,.F.);
#4668=ORIENTED_EDGE('',*,*,#3311,.T.);
#4669=ORIENTED_EDGE('',*,*,#3309,.F.);
#4670=ORIENTED_EDGE('',*,*,#3311,.F.);
#4671=ORIENTED_EDGE('',*,*,#3310,.T.);
#5273=CYLINDRICAL_SURFACE('',#6424,4.925);
#5594=ADVANCED_FACE('',(#651),#357,.F.);
#5595=ADVANCED_FACE('',(#652),#5273,.T.);
#5596=ADVANCED_FACE('',(#653),#358,.T.);
#5717=CLOSED_SHELL('',(#5594,#5595,#5596));
#6421=AXIS2_PLACEMENT_3D('',#9998,#8105,#8106);
#6422=AXIS2_PLACEMENT_3D('',#9999,#8107,#8108);
#6423=AXIS2_PLACEMENT_3D('',#10001,#8109,#8110);
#6424=AXIS2_PLACEMENT_3D('',#10002,#8111,#8112);
#6425=AXIS2_PLACEMENT_3D('',#10004,#8113,#8114);
#6426=AXIS2_PLACEMENT_3D('',#10006,#8116,#8117);
#8105=DIRECTION('axis',(0.,0.,1.));
#8106=DIRECTION('refdir',(1.,0.,0.));
#8107=DIRECTION('center_axis',(-1.,0.,0.));
#8108=DIRECTION('ref_axis',(0.,-1.,0.));
#8109=DIRECTION('center_axis',(1.,0.,0.));
#8110=DIRECTION('ref_axis',(0.,-1.,0.));
#8111=DIRECTION('center_axis',(-1.,0.,0.));
#8112=DIRECTION('ref_axis',(0.,-1.,0.));
#8113=DIRECTION('center_axis',(1.,0.,0.));
#8114=DIRECTION('ref_axis',(0.,-1.,0.));
#8115=DIRECTION('',(1.,0.,0.));
#8116=DIRECTION('center_axis',(-1.,0.,0.));
#8117=DIRECTION('ref_axis',(0.,-1.,0.));
#9998=CARTESIAN_POINT('',(0.,0.,0.));
#9999=CARTESIAN_POINT('Origin',(129.,0.,0.));
#10000=CARTESIAN_POINT('',(129.,4.925,6.03138548580071E-16));
#10001=CARTESIAN_POINT('Origin',(129.,0.,0.));
#10002=CARTESIAN_POINT('Origin',(-125.,0.,0.));
#10003=CARTESIAN_POINT('',(-129.,4.925,6.03138548580071E-16));
#10004=CARTESIAN_POINT('Origin',(-129.,0.,0.));
#10005=CARTESIAN_POINT('',(-125.,4.925,-6.03138548580071E-16));
#10006=CARTESIAN_POINT('Origin',(-129.,0.,0.));
#10621=UNCERTAINTY_MEASURE_WITH_UNIT(LENGTH_MEASURE(0.01),#10640,
'DISTANCE_ACCURACY_VALUE',
'Maximum model space distance between geometric entities at asserted c
onnectivities');
#10627=UNCERTAINTY_MEASURE_WITH_UNIT(LENGTH_MEASURE(0.01),#10640,
'DISTANCE_ACCURACY_VALUE',
'Maximum model space distance between geometric entities at asserted c
onnectivities');
#10633=(
GEOMETRIC_REPRESENTATION_CONTEXT(3)
GLOBAL_UNCERTAINTY_ASSIGNED_CONTEXT((#10621))
GLOBAL_UNIT_ASSIGNED_CONTEXT((#10640,#10642,#10643))
REPRESENTATION_CONTEXT('','3D')
);
#10639=(
GEOMETRIC_REPRESENTATION_CONTEXT(3)
GLOBAL_UNCERTAINTY_ASSIGNED_CONTEXT((#10627))
GLOBAL_UNIT_ASSIGNED_CONTEXT((#10640,#10642,#10643))
REPRESENTATION_CONTEXT('','3D')
);
#10640=(
LENGTH_UNIT()
NAMED_UNIT(*)
SI_UNIT(.MILLI.,.METRE.)
);
#10642=(
NAMED_UNIT(*)
PLANE_ANGLE_UNIT()
SI_UNIT($,.RADIAN.)
);
#10643=(
NAMED_UNIT(*)
SI_UNIT($,.STERADIAN.)
SOLID_ANGLE_UNIT()
);
#10649=SHAPE_DEFINITION_REPRESENTATION(#10660,#10681);
#10660=PRODUCT_DEFINITION_SHAPE('',$,#10693);
#10681=SHAPE_REPRESENTATION('',(#6421),#10633);
#10687=PRODUCT_DEFINITION_CONTEXT('part definition',#10722,'design');
#10693=PRODUCT_DEFINITION('Screw','Screw',#10704,#10687);
#10704=PRODUCT_DEFINITION_FORMATION('',$,#10729);
#10722=APPLICATION_CONTEXT(
'Core Data for Automotive Mechanical Design Process');
#10723=PRODUCT_CONTEXT('part definition',#10722,'mechanical');
#10729=PRODUCT('Screw','Screw',$,(#10723));
#10791=COLOUR_RGB('Black',0.12,0.14,0.17);
#10792=FILL_AREA_STYLE_COLOUR('',#10791);
#10793=FILL_AREA_STYLE('',(#10792));
#10794=SURFACE_STYLE_FILL_AREA(#10793);
#10795=SURFACE_SIDE_STYLE('',(#10794));
#10796=SURFACE_STYLE_USAGE(.BOTH.,#10795);
#10797=PRESENTATION_STYLE_ASSIGNMENT((#10796));
ENDSEC;
END-ISO-10303-21;
